ISO-10303-21;
HEADER;
/* Generated by software containing ST-Developer
 * from STEP Tools, Inc. (www.steptools.com) 
 */

FILE_DESCRIPTION(
/* description */ ('Pallet stop with pneumatic fitting'),
/* implementation_level */ '2;1');

FILE_NAME(
/* name */ 'M4x4 shaft screw.step',
/* time_stamp */ '2026-10-27T10:51:41-07:00',
/* author */ (''),
/* organization */ (''),
/* preprocessor_version */ 'ST-DEVELOPER v20.2',
/* originating_system */ 'Autodesk Translation Framework v15.17.0.0',
/* authorisation */ '');

FILE_SCHEMA (('AUTOMOTIVE_DESIGN { 1 0 10303 214 3 1 1 }'));
ENDSEC;

DATA;
#10=MECHANICAL_DESIGN_GEOMETRIC_PRESENTATION_REPRESENTATION('',(#387),#10265);
#33=CONICAL_SURFACE('',#6004,0.185,0.785398163397449);
#323=SHAPE_REPRESENTATION_RELATIONSHIP('SRR','None',#10439,#355);
#355=ADVANCED_BREP_SHAPE_REPRESENTATION('',(#418),#10263);
#387=STYLED_ITEM('',(#10662),#418);
#418=MANIFOLD_SOLID_BREP('Body1',#5076);
#543=FACE_BOUND('',#1469,.T.);
#716=PLANE('',#5993);
#717=PLANE('',#5995);
#718=PLANE('',#5996);
#719=PLANE('',#5997);
#720=PLANE('',#5998);
#721=PLANE('',#5999);
#722=PLANE('',#6000);
#723=PLANE('',#6001);
#724=PLANE('',#6002);
#1022=FACE_OUTER_BOUND('',#1460,.T.);
#1023=FACE_OUTER_BOUND('',#1461,.T.);
#1024=FACE_OUTER_BOUND('',#1462,.T.);
#1025=FACE_OUTER_BOUND('',#1463,.T.);
#1026=FACE_OUTER_BOUND('',#1464,.T.);
#1027=FACE_OUTER_BOUND('',#1465,.T.);
#1028=FACE_OUTER_BOUND('',#1466,.T.);
#1029=FACE_OUTER_BOUND('',#1467,.T.);
#1030=FACE_OUTER_BOUND('',#1468,.T.);
#1031=FACE_OUTER_BOUND('',#1470,.T.);
#1032=FACE_OUTER_BOUND('',#1471,.T.);
#1460=EDGE_LOOP('',(#4512));
#1461=EDGE_LOOP('',(#4513,#4514,#4515,#4516));
#1462=EDGE_LOOP('',(#4517,#4518,#4519,#4520));
#1463=EDGE_LOOP('',(#4521,#4522,#4523,#4524));
#1464=EDGE_LOOP('',(#4525,#4526,#4527,#4528));
#1465=EDGE_LOOP('',(#4529,#4530,#4531,#4532));
#1466=EDGE_LOOP('',(#4533,#4534,#4535,#4536));
#1467=EDGE_LOOP('',(#4537,#4538,#4539,#4540,#4541,#4542));
#1468=EDGE_LOOP('',(#4543));
#1469=EDGE_LOOP('',(#4544,#4545,#4546,#4547,#4548,#4549));
#1470=EDGE_LOOP('',(#4550,#4551,#4552,#4553));
#1471=EDGE_LOOP('',(#4554,#4555,#4556,#4557));
#1781=LINE('',#10021,#2116);
#1782=LINE('',#10023,#2117);
#1783=LINE('',#10025,#2118);
#1784=LINE('',#10026,#2119);
#1785=LINE('',#10029,#2120);
#1786=LINE('',#10031,#2121);
#1787=LINE('',#10032,#2122);
#1788=LINE('',#10035,#2123);
#1789=LINE('',#10037,#2124);
#1790=LINE('',#10038,#2125);
#1791=LINE('',#10041,#2126);
#1792=LINE('',#10043,#2127);
#1793=LINE('',#10044,#2128);
#1794=LINE('',#10047,#2129);
#1795=LINE('',#10049,#2130);
#1796=LINE('',#10050,#2131);
#1797=LINE('',#10052,#2132);
#1798=LINE('',#10053,#2133);
#1799=LINE('',#10061,#2134);
#1800=LINE('',#10063,#2135);
#2116=VECTOR('',#7508,1.);
#2117=VECTOR('',#7509,1.);
#2118=VECTOR('',#7510,1.);
#2119=VECTOR('',#7511,1.);
#2120=VECTOR('',#7514,1.);
#2121=VECTOR('',#7515,1.);
#2122=VECTOR('',#7516,1.);
#2123=VECTOR('',#7519,1.);
#2124=VECTOR('',#7520,1.);
#2125=VECTOR('',#7521,1.);
#2126=VECTOR('',#7524,1.);
#2127=VECTOR('',#7525,1.);
#2128=VECTOR('',#7526,1.);
#2129=VECTOR('',#7529,1.);
#2130=VECTOR('',#7530,1.);
#2131=VECTOR('',#7531,1.);
#2132=VECTOR('',#7534,1.);
#2133=VECTOR('',#7535,1.);
#2134=VECTOR('',#7546,0.185);
#2135=VECTOR('',#7549,0.2);
#2396=CIRCLE('',#5994,0.1954);
#2397=CIRCLE('',#6003,0.17);
#2398=CIRCLE('',#6005,0.1954);
#2769=VERTEX_POINT('',#10016);
#2770=VERTEX_POINT('',#10019);
#2771=VERTEX_POINT('',#10020);
#2772=VERTEX_POINT('',#10022);
#2773=VERTEX_POINT('',#10024);
#2774=VERTEX_POINT('',#10028);
#2775=VERTEX_POINT('',#10030);
#2776=VERTEX_POINT('',#10034);
#2777=VERTEX_POINT('',#10036);
#2778=VERTEX_POINT('',#10040);
#2779=VERTEX_POINT('',#10042);
#2780=VERTEX_POINT('',#10046);
#2781=VERTEX_POINT('',#10048);
#2782=VERTEX_POINT('',#10056);
#2783=VERTEX_POINT('',#10059);
#3355=EDGE_CURVE('',#2769,#2769,#2396,.T.);
#3356=EDGE_CURVE('',#2770,#2771,#1781,.T.);
#3357=EDGE_CURVE('',#2770,#2772,#1782,.T.);
#3358=EDGE_CURVE('',#2772,#2773,#1783,.T.);
#3359=EDGE_CURVE('',#2771,#2773,#1784,.T.);
#3360=EDGE_CURVE('',#2774,#2770,#1785,.T.);
#3361=EDGE_CURVE('',#2774,#2775,#1786,.T.);
#3362=EDGE_CURVE('',#2775,#2772,#1787,.T.);
#3363=EDGE_CURVE('',#2776,#2774,#1788,.T.);
#3364=EDGE_CURVE('',#2776,#2777,#1789,.T.);
#3365=EDGE_CURVE('',#2777,#2775,#1790,.T.);
#3366=EDGE_CURVE('',#2778,#2776,#1791,.T.);
#3367=EDGE_CURVE('',#2778,#2779,#1792,.T.);
#3368=EDGE_CURVE('',#2779,#2777,#1793,.T.);
#3369=EDGE_CURVE('',#2780,#2778,#1794,.T.);
#3370=EDGE_CURVE('',#2780,#2781,#1795,.T.);
#3371=EDGE_CURVE('',#2781,#2779,#1796,.T.);
#3372=EDGE_CURVE('',#2771,#2780,#1797,.T.);
#3373=EDGE_CURVE('',#2773,#2781,#1798,.T.);
#3374=EDGE_CURVE('',#2782,#2782,#2397,.T.);
#3375=EDGE_CURVE('',#2783,#2783,#2398,.T.);
#3376=EDGE_CURVE('',#2783,#2782,#1799,.T.);
#3377=EDGE_CURVE('',#2769,#2783,#1800,.T.);
#4512=ORIENTED_EDGE('',*,*,#3355,.F.);
#4513=ORIENTED_EDGE('',*,*,#3356,.F.);
#4514=ORIENTED_EDGE('',*,*,#3357,.T.);
#4515=ORIENTED_EDGE('',*,*,#3358,.T.);
#4516=ORIENTED_EDGE('',*,*,#3359,.F.);
#4517=ORIENTED_EDGE('',*,*,#3360,.F.);
#4518=ORIENTED_EDGE('',*,*,#3361,.T.);
#4519=ORIENTED_EDGE('',*,*,#3362,.T.);
#4520=ORIENTED_EDGE('',*,*,#3357,.F.);
#4521=ORIENTED_EDGE('',*,*,#3363,.F.);
#4522=ORIENTED_EDGE('',*,*,#3364,.T.);
#4523=ORIENTED_EDGE('',*,*,#3365,.T.);
#4524=ORIENTED_EDGE('',*,*,#3361,.F.);
#4525=ORIENTED_EDGE('',*,*,#3366,.F.);
#4526=ORIENTED_EDGE('',*,*,#3367,.T.);
#4527=ORIENTED_EDGE('',*,*,#3368,.T.);
#4528=ORIENTED_EDGE('',*,*,#3364,.F.);
#4529=ORIENTED_EDGE('',*,*,#3369,.F.);
#4530=ORIENTED_EDGE('',*,*,#3370,.T.);
#4531=ORIENTED_EDGE('',*,*,#3371,.T.);
#4532=ORIENTED_EDGE('',*,*,#3367,.F.);
#4533=ORIENTED_EDGE('',*,*,#3372,.F.);
#4534=ORIENTED_EDGE('',*,*,#3359,.T.);
#4535=ORIENTED_EDGE('',*,*,#3373,.T.);
#4536=ORIENTED_EDGE('',*,*,#3370,.F.);
#4537=ORIENTED_EDGE('',*,*,#3373,.F.);
#4538=ORIENTED_EDGE('',*,*,#3358,.F.);
#4539=ORIENTED_EDGE('',*,*,#3362,.F.);
#4540=ORIENTED_EDGE('',*,*,#3365,.F.);
#4541=ORIENTED_EDGE('',*,*,#3368,.F.);
#4542=ORIENTED_EDGE('',*,*,#3371,.F.);
#4543=ORIENTED_EDGE('',*,*,#3374,.F.);
#4544=ORIENTED_EDGE('',*,*,#3356,.T.);
#4545=ORIENTED_EDGE('',*,*,#3372,.T.);
#4546=ORIENTED_EDGE('',*,*,#3369,.T.);
#4547=ORIENTED_EDGE('',*,*,#3366,.T.);
#4548=ORIENTED_EDGE('',*,*,#3363,.T.);
#4549=ORIENTED_EDGE('',*,*,#3360,.T.);
#4550=ORIENTED_EDGE('',*,*,#3375,.F.);
#4551=ORIENTED_EDGE('',*,*,#3376,.T.);
#4552=ORIENTED_EDGE('',*,*,#3374,.T.);
#4553=ORIENTED_EDGE('',*,*,#3376,.F.);
#4554=ORIENTED_EDGE('',*,*,#3355,.T.);
#4555=ORIENTED_EDGE('',*,*,#3377,.T.);
#4556=ORIENTED_EDGE('',*,*,#3375,.T.);
#4557=ORIENTED_EDGE('',*,*,#3377,.F.);
#4728=CYLINDRICAL_SURFACE('',#6006,0.1954);
#5017=ADVANCED_FACE('',(#1022),#716,.F.);
#5018=ADVANCED_FACE('',(#1023),#717,.F.);
#5019=ADVANCED_FACE('',(#1024),#718,.F.);
#5020=ADVANCED_FACE('',(#1025),#719,.F.);
#5021=ADVANCED_FACE('',(#1026),#720,.F.);
#5022=ADVANCED_FACE('',(#1027),#721,.F.);
#5023=ADVANCED_FACE('',(#1028),#722,.F.);
#5024=ADVANCED_FACE('',(#1029),#723,.F.);
#5025=ADVANCED_FACE('',(#1030,#543),#724,.T.);
#5026=ADVANCED_FACE('',(#1031),#33,.T.);
#5027=ADVANCED_FACE('',(#1032),#4728,.T.);
#5076=CLOSED_SHELL('',(#5017,#5018,#5019,#5020,#5021,#5022,#5023,#5024,
#5025,#5026,#5027));
#5992=AXIS2_PLACEMENT_3D('',#10014,#7500,#7501);
#5993=AXIS2_PLACEMENT_3D('',#10015,#7502,#7503);
#5994=AXIS2_PLACEMENT_3D('',#10017,#7504,#7505);
#5995=AXIS2_PLACEMENT_3D('',#10018,#7506,#7507);
#5996=AXIS2_PLACEMENT_3D('',#10027,#7512,#7513);
#5997=AXIS2_PLACEMENT_3D('',#10033,#7517,#7518);
#5998=AXIS2_PLACEMENT_3D('',#10039,#7522,#7523);
#5999=AXIS2_PLACEMENT_3D('',#10045,#7527,#7528);
#6000=AXIS2_PLACEMENT_3D('',#10051,#7532,#7533);
#6001=AXIS2_PLACEMENT_3D('',#10054,#7536,#7537);
#6002=AXIS2_PLACEMENT_3D('',#10055,#7538,#7539);
#6003=AXIS2_PLACEMENT_3D('',#10057,#7540,#7541);
#6004=AXIS2_PLACEMENT_3D('',#10058,#7542,#7543);
#6005=AXIS2_PLACEMENT_3D('',#10060,#7544,#7545);
#6006=AXIS2_PLACEMENT_3D('',#10062,#7547,#7548);
#7500=DIRECTION('axis',(0.,0.,1.));
#7501=DIRECTION('refdir',(1.,0.,0.));
#7502=DIRECTION('center_axis',(0.,1.,0.));
#7503=DIRECTION('ref_axis',(1.,0.,0.));
#7504=DIRECTION('center_axis',(0.,1.,0.));
#7505=DIRECTION('ref_axis',(1.,0.,0.));
#7506=DIRECTION('center_axis',(0.866025403784439,0.,-0.5));
#7507=DIRECTION('ref_axis',(0.5,0.,0.866025403784439));
#7508=DIRECTION('',(0.5,0.,0.866025403784439));
#7509=DIRECTION('',(0.,-1.,0.));
#7510=DIRECTION('',(0.5,0.,0.866025403784439));
#7511=DIRECTION('',(0.,-1.,0.));
#7512=DIRECTION('center_axis',(1.20185167898973E-16,0.,-1.));
#7513=DIRECTION('ref_axis',(1.,0.,1.20185167898973E-16));
#7514=DIRECTION('',(1.,0.,1.20185167898973E-16));
#7515=DIRECTION('',(0.,-1.,0.));
#7516=DIRECTION('',(1.,0.,1.20185167898973E-16));
#7517=DIRECTION('center_axis',(-0.866025403784439,0.,-0.5));
#7518=DIRECTION('ref_axis',(0.5,0.,-0.866025403784439));
#7519=DIRECTION('',(0.5,0.,-0.866025403784439));
#7520=DIRECTION('',(0.,-1.,0.));
#7521=DIRECTION('',(0.5,0.,-0.866025403784439));
#7522=DIRECTION('center_axis',(-0.866025403784439,0.,0.5));
#7523=DIRECTION('ref_axis',(-0.5,0.,-0.866025403784439));
#7524=DIRECTION('',(-0.5,0.,-0.866025403784439));
#7525=DIRECTION('',(0.,-1.,0.));
#7526=DIRECTION('',(-0.5,0.,-0.866025403784439));
#7527=DIRECTION('center_axis',(-2.40370335797945E-16,0.,1.));
#7528=DIRECTION('ref_axis',(-1.,0.,-2.40370335797945E-16));
#7529=DIRECTION('',(-1.,0.,-2.40370335797945E-16));
#7530=DIRECTION('',(0.,-1.,0.));
#7531=DIRECTION('',(-1.,0.,-2.40370335797945E-16));
#7532=DIRECTION('center_axis',(0.866025403784439,0.,0.5));
#7533=DIRECTION('ref_axis',(-0.5,0.,0.866025403784439));
#7534=DIRECTION('',(-0.5,0.,0.866025403784439));
#7535=DIRECTION('',(-0.5,0.,0.866025403784439));
#7536=DIRECTION('center_axis',(0.,-1.,0.));
#7537=DIRECTION('ref_axis',(0.,0.,-1.));
#7538=DIRECTION('center_axis',(0.,1.,0.));
#7539=DIRECTION('ref_axis',(0.,0.,1.));
#7540=DIRECTION('center_axis',(0.,-1.,0.));
#7541=DIRECTION('ref_axis',(1.,0.,0.));
#7542=DIRECTION('center_axis',(0.,-1.,0.));
#7543=DIRECTION('ref_axis',(1.,0.,0.));
#7544=DIRECTION('center_axis',(0.,-1.,0.));
#7545=DIRECTION('ref_axis',(1.,0.,0.));
#7546=DIRECTION('',(0.707106781186548,0.707106781186547,8.65956056235494E-17));
#7547=DIRECTION('center_axis',(0.,-1.,0.));
#7548=DIRECTION('ref_axis',(1.,0.,0.));
#7549=DIRECTION('',(0.,1.,0.));
#10014=CARTESIAN_POINT('',(0.,0.,0.));
#10015=CARTESIAN_POINT('Origin',(0.,-0.4,0.));
#10016=CARTESIAN_POINT('',(-0.1954,-0.4,2.39295984553393E-17));
#10017=CARTESIAN_POINT('Origin',(0.,-0.4,0.));
#10018=CARTESIAN_POINT('Origin',(0.0577350269189626,0.,-0.1));
#10019=CARTESIAN_POINT('',(0.0577350269189626,0.,-0.1));
#10020=CARTESIAN_POINT('',(0.115470053837925,0.,0.));
#10021=CARTESIAN_POINT('',(0.0934187836487032,0.,-0.0381939203391614));
#10022=CARTESIAN_POINT('',(0.0577350269189626,-0.2,-0.1));
#10023=CARTESIAN_POINT('',(0.0577350269189626,0.,-0.1));
#10024=CARTESIAN_POINT('',(0.115470053837925,-0.2,0.));
#10025=CARTESIAN_POINT('',(0.115470053837925,-0.2,0.));
#10026=CARTESIAN_POINT('',(0.115470053837925,0.,0.));
#10027=CARTESIAN_POINT('Origin',(-0.0577350269189626,0.,-0.1));
#10028=CARTESIAN_POINT('',(-0.0577350269189626,0.,-0.1));
#10029=CARTESIAN_POINT('',(0.0561324865405187,0.,-0.1));
#10030=CARTESIAN_POINT('',(-0.0577350269189626,-0.2,-0.1));
#10031=CARTESIAN_POINT('',(-0.0577350269189626,0.,-0.1));
#10032=CARTESIAN_POINT('',(0.0577350269189626,-0.2,-0.1));
#10033=CARTESIAN_POINT('Origin',(-0.115470053837925,0.,-1.38777878078145E-17));
#10034=CARTESIAN_POINT('',(-0.115470053837925,0.,-1.41410031829988E-17));
#10035=CARTESIAN_POINT('',(-0.0797862971081845,0.,-0.0618060796608387));
#10036=CARTESIAN_POINT('',(-0.115470053837925,-0.2,-1.38777878078145E-17));
#10037=CARTESIAN_POINT('',(-0.115470053837925,0.,-1.41410031829988E-17));
#10038=CARTESIAN_POINT('',(-0.0577350269189626,-0.2,-0.1));
#10039=CARTESIAN_POINT('Origin',(-0.0577350269189626,0.,0.1));
#10040=CARTESIAN_POINT('',(-0.0577350269189626,0.,0.1));
#10041=CARTESIAN_POINT('',(-0.0509187836487033,0.,0.111806079660839));
#10042=CARTESIAN_POINT('',(-0.0577350269189626,-0.2,0.1));
#10043=CARTESIAN_POINT('',(-0.0577350269189626,0.,0.1));
#10044=CARTESIAN_POINT('',(-0.115470053837925,-0.2,-1.41410031829988E-17));
#10045=CARTESIAN_POINT('Origin',(0.0577350269189626,0.,0.1));
#10046=CARTESIAN_POINT('',(0.0577350269189626,0.,0.1));
#10047=CARTESIAN_POINT('',(0.113867513459481,0.,0.1));
#10048=CARTESIAN_POINT('',(0.0577350269189626,-0.2,0.1));
#10049=CARTESIAN_POINT('',(0.0577350269189626,0.,0.1));
#10050=CARTESIAN_POINT('',(-0.0577350269189626,-0.2,0.1));
#10051=CARTESIAN_POINT('Origin',(0.115470053837925,0.,0.));
#10052=CARTESIAN_POINT('',(0.122286297108185,0.,-0.0118060796608386));
#10053=CARTESIAN_POINT('',(0.0577350269189626,-0.2,0.1));
#10054=CARTESIAN_POINT('Origin',(0.,-0.2,0.));
#10055=CARTESIAN_POINT('Origin',(0.17,0.,0.));
#10056=CARTESIAN_POINT('',(-0.17,-8.67361737988404E-18,-2.0818995585505E-17));
#10057=CARTESIAN_POINT('Origin',(0.,0.,0.));
#10058=CARTESIAN_POINT('Origin',(0.,-0.015,0.));
#10059=CARTESIAN_POINT('',(-0.1954,-0.0254,-2.39295984553393E-17));
#10060=CARTESIAN_POINT('Origin',(0.,-0.0254,0.));
#10061=CARTESIAN_POINT('',(-0.185,-0.015,-2.2655965784226E-17));
#10062=CARTESIAN_POINT('Origin',(0.,-0.2775,0.));
#10063=CARTESIAN_POINT('',(-0.1954,-0.2775,-2.39295984553393E-17));
#10225=UNCERTAINTY_MEASURE_WITH_UNIT(LENGTH_MEASURE(0.001),#10266,
'DISTANCE_ACCURACY_VALUE',
'Maximum model space distance between geometric entities at asserted c
onnectivities');
#10227=UNCERTAINTY_MEASURE_WITH_UNIT(LENGTH_MEASURE(0.001),#10266,
'DISTANCE_ACCURACY_VALUE',
'Maximum model space distance between geometric entities at asserted c
onnectivities');
#10263=(
GEOMETRIC_REPRESENTATION_CONTEXT(3)
GLOBAL_UNCERTAINTY_ASSIGNED_CONTEXT((#10225))
GLOBAL_UNIT_ASSIGNED_CONTEXT((#10266,#10268,#10269))
REPRESENTATION_CONTEXT('','3D')
);
#10265=(
GEOMETRIC_REPRESENTATION_CONTEXT(3)
GLOBAL_UNCERTAINTY_ASSIGNED_CONTEXT((#10227))
GLOBAL_UNIT_ASSIGNED_CONTEXT((#10266,#10268,#10269))
REPRESENTATION_CONTEXT('','3D')
);
#10266=(
LENGTH_UNIT()
NAMED_UNIT(*)
SI_UNIT(.CENTI.,.METRE.)
);
#10268=(
NAMED_UNIT(*)
PLANE_ANGLE_UNIT()
SI_UNIT($,.RADIAN.)
);
#10269=(
NAMED_UNIT(*)
SI_UNIT($,.STERADIAN.)
SOLID_ANGLE_UNIT()
);
#10305=SHAPE_DEFINITION_REPRESENTATION(#10346,#10439);
#10346=PRODUCT_DEFINITION_SHAPE('',$,#10477);
#10439=SHAPE_REPRESENTATION('',(#5992),#10263);
#10441=PRODUCT_DEFINITION_CONTEXT('part definition',#10554,'design');
#10477=PRODUCT_DEFINITION('M4x4 shaft screw','M4x4 shaft screw',#10514,
#10441);
#10514=PRODUCT_DEFINITION_FORMATION('',$,#10591);
#10554=APPLICATION_CONTEXT(
'Core Data for Automotive Mechanical Design Process');
#10555=PRODUCT_CONTEXT('part definition',#10554,'mechanical');
#10591=PRODUCT('M4x4 shaft screw','M4x4 shaft screw','M4x4 shaft screw',
(#10555));
#10656=COLOUR_RGB('Black',0.12,0.14,0.17);
#10657=FILL_AREA_STYLE_COLOUR('',#10656);
#10658=FILL_AREA_STYLE('',(#10657));
#10659=SURFACE_STYLE_FILL_AREA(#10658);
#10660=SURFACE_SIDE_STYLE('',(#10659));
#10661=SURFACE_STYLE_USAGE(.BOTH.,#10660);
#10662=PRESENTATION_STYLE_ASSIGNMENT((#10661));
ENDSEC;
END-ISO-10303-21;
